ISO-10303-21;
HEADER;
FILE_DESCRIPTION (('STEP AP203'),
    '1' );
FILE_NAME ('bench vise9-.step',
    '2026-10-07T23:37:23',
    ( '' ),
    ( '' ),
    'SwSTEP 2.0',
    'SolidWorks 2024',
    '' );
FILE_SCHEMA (( 'AUTOMOTIVE_DESIGN' ));
ENDSEC;

DATA;
#46=CARTESIAN_POINT ( 'NONE',  ( -0.7335374419612978869, 3.792759758930658531, 8.502074107329825381 ) ) ;
#70=EDGE_LOOP ( 'NONE', ( #2555, #6227 ) ) ;
#96=SHAPE_DEFINITION_REPRESENTATION ( #1706, #2780 ) ;
#109=B_SPLINE_CURVE_WITH_KNOTS ( 'NONE', 3,
 ( #7082, #3263, #3389, #1429, #5254, #2158, #2655, #2036, #5139, #5854, #6561, #3992, #235, #929, #7685, #3940, #3903, #2080, #4572, #1464, #6222, #3185, #4487, #140, #5807, #5908, #7147, #1492, #3971, #260, #7791, #6408, #825, #7023, #3369, #6543, #3328, #1535, #1412, #2138, #7710, #954, #5832, #214 ),
 .UNSPECIFIED., .F., .F.,
 ( 4, 2, 2, 2, 2, 2, 2, 2, 2, 2, 2, 2, 2, 2, 2, 2, 2, 2, 2, 2, 2, 4 ),
 ( 1.387778780781445676E-17, 0.001568404162335165731, 0.002352606243502761499, 0.003136808324670357917, 0.004705212487005582846, 0.005489414568173214826, 0.006273616649340845071, 0.007842020811676163675, 0.009410424974011483146, 0.01019462705517914375, 0.01097882913634680262, 0.01254723329868211515, 0.01333143537984972891, 0.01411563746101734441, 0.01568404162335264307, 0.01725244578568794346, 0.01882084994802324038, 0.02038925411035854424, 0.02117345619152621525, 0.02195765827269388973, 0.02352606243502923522, 0.02509446659736457724 ),
 .UNSPECIFIED. ) ;
#114=FACE_OUTER_BOUND ( 'NONE', #4631, .T. ) ;
#140=CARTESIAN_POINT ( 'NONE',  ( 0.6817881100752517520, 3.637486043182223128, 8.241141111267671349 ) ) ;
#149=SHAPE_REPRESENTATION_RELATIONSHIP ( 'NONE' , 'NONE' ,  #2780, #2140 ) ;
#172=CARTESIAN_POINT ( 'NONE',  ( -0.7274884641267203023, 3.767418641134390178, 8.485068404623115512 ) ) ;
#214=CARTESIAN_POINT ( 'NONE',  ( 0.7499999999999993339, 3.950000000000000178, 8.543750000000002842 ) ) ;
#235=CARTESIAN_POINT ( 'NONE',  ( 0.7188803599037367764, 3.736068989823151387, 8.003234414602296454 ) ) ;
#245=( LENGTH_UNIT ( ) NAMED_UNIT ( * ) SI_UNIT ( $, .METRE. ) );
#260=CARTESIAN_POINT ( 'NONE',  ( 0.6955978521287337069, 3.669434091866876635, 8.370402240390431459 ) ) ;
#352=CARTESIAN_POINT ( 'NONE',  ( 0.6863513793485910286, 4.252392623524238857, 8.149781182892043674 ) ) ;
#378=DESIGN_CONTEXT ( 'detailed design', #6135, 'design' ) ;
#394=CARTESIAN_POINT ( 'NONE',  ( 0.6827599196736721110, 4.260417128052496949, 8.272753927050754186 ) ) ;
#418=DIRECTION ( 'NONE',  ( 0.000000000000000000, 0.000000000000000000, 1.000000000000000000 ) ) ;
#422=DIRECTION ( 'NONE',  ( 1.000000000000000000, 0.000000000000000000, 0.000000000000000000 ) ) ;
#432=AXIS2_PLACEMENT_3D ( 'NONE', #2468, #8085, #6350 ) ;
#453=CARTESIAN_POINT ( 'NONE',  ( -0.7274884641267199692, 4.132581358865608401, 7.977431595376885731 ) ) ;
#503=DIRECTION ( 'NONE',  ( 0.000000000000000000, 0.000000000000000000, -1.000000000000000000 ) ) ;
#529=CARTESIAN_POINT ( 'NONE',  ( -0.7499999999999993339, 3.950000000000000622, 8.543750000000002842 ) ) ;
#567=CARTESIAN_POINT ( 'NONE',  ( -0.7335374419612978869, 4.107240241069344044, 7.960425892670178527 ) ) ;
#616=CARTESIAN_POINT ( 'NONE',  ( -0.7333924044284368948, 4.107224863919222813, 8.501510692915040579 ) ) ;
#639=CARTESIAN_POINT ( 'NONE',  ( -0.7431911064911159714, 3.848678615087431698, 8.527048809074745606 ) ) ;
#649=DIRECTION ( 'NONE',  ( 0.000000000000000000, 0.000000000000000000, 1.000000000000000000 ) ) ;
#685=DIRECTION ( 'NONE',  ( -1.000000000000000000, -0.000000000000000000, -0.000000000000000000 ) ) ;
#767=LINE ( 'NONE', #5022, #3826 ) ;
#778=LENGTH_MEASURE_WITH_UNIT ( LENGTH_MEASURE( 0.02539999999999999897 ), #245 );
#798=ORIENTED_EDGE ( 'NONE', *, *, #7951, .T. ) ;
#823=CARTESIAN_POINT ( 'NONE',  ( -0.7499999999999995559, 3.929097005416127608, 7.918750000000000178 ) ) ;
#825=CARTESIAN_POINT ( 'NONE',  ( 0.7122575715994515777, 3.714602561338662401, 8.437773039678205578 ) ) ;
#826=VECTOR ( 'NONE', #6076, 39.37007874015748143 ) ;
#835=AXIS2_PLACEMENT_3D ( 'NONE', #4211, #503, #1157 ) ;
#840=ADVANCED_FACE ( 'NONE', ( #2198 ), #2152, .T. ) ;
#859=DIRECTION ( 'NONE',  ( 1.000000000000000000, 0.000000000000000000, -0.000000000000000000 ) ) ;
#889=CARTESIAN_POINT ( 'NONE',  ( 0.7499999999999993339, 3.950000000000000178, 8.831250000000000711 ) ) ;
#929=CARTESIAN_POINT ( 'NONE',  ( 0.7122963468828457101, 3.714722057770372565, 8.024595996655376595 ) ) ;
#931=DIRECTION ( 'NONE',  ( -1.000000000000000000, -0.000000000000000000, -0.000000000000000000 ) ) ;
#938=VERTEX_POINT ( 'NONE', #7905 ) ;
#943=EDGE_CURVE ( 'NONE', #3948, #8045, #8127, .T. ) ;
#952=ORIENTED_EDGE ( 'NONE', *, *, #6340, .T. ) ;
#954=CARTESIAN_POINT ( 'NONE',  ( 0.7491228847736894902, 3.908369212101149071, 8.541661844804181669 ) ) ;
#977=CARTESIAN_POINT ( 'NONE',  ( 0.6818077110526902240, 4.262471192484426297, 8.252326836086270490 ) ) ;
#982=AXIS2_PLACEMENT_3D ( 'NONE', #6039, #6734, #422 ) ;
#1024=ORIENTED_EDGE ( 'NONE', *, *, #1386, .T. ) ;
#1047=CARTESIAN_POINT ( 'NONE',  ( -0.6892550738286248313, 3.654300326837817803, 8.332856313163134132 ) ) ;
#1061=FACE_OUTER_BOUND ( 'NONE', #2906, .T. ) ;
#1071=CARTESIAN_POINT ( 'NONE',  ( -0.7370170160409599269, 4.089247961470974246, 8.511197325751677312 ) ) ;
#1111=CARTESIAN_POINT ( 'NONE',  ( -0.7210672075785411472, 4.156465442921959408, 7.996449899345011048 ) ) ;
#1115=CIRCLE ( 'NONE', #982, 0.7499999999999993339 ) ;
#1121=ORIENTED_EDGE ( 'NONE', *, *, #8052, .T. ) ;
#1124=ORIENTED_EDGE ( 'NONE', *, *, #4724, .F. ) ;
#1157=DIRECTION ( 'NONE',  ( -1.000000000000000000, 0.000000000000000000, -0.000000000000000000 ) ) ;
#1158=CARTESIAN_POINT ( 'NONE',  ( -0.7499999999999993339, 3.950000000000000178, 8.831250000000000711 ) ) ;
#1200=EDGE_CURVE ( 'NONE', #8086, #4460, #4135, .T. ) ;
#1224=CARTESIAN_POINT ( 'NONE',  ( -0.6827599196736721110, 4.260417128052496949, 8.189746072949246170 ) ) ;
#1321=DIRECTION ( 'NONE',  ( 1.000000000000000000, 0.000000000000000000, 0.000000000000000000 ) ) ;
#1331=ORIENTED_EDGE ( 'NONE', *, *, #2877, .F. ) ;
#1380=( GEOMETRIC_REPRESENTATION_CONTEXT ( 3 ) GLOBAL_UNCERTAINTY_ASSIGNED_CONTEXT ( ( #6450 ) ) GLOBAL_UNIT_ASSIGNED_CONTEXT ( ( #7737, #4617, #2125 ) ) REPRESENTATION_CONTEXT ( 'NONE', 'WORKASPACE' ) );
#1386=EDGE_CURVE ( 'NONE', #2452, #5045, #3496, .T. ) ;
#1408=CARTESIAN_POINT ( 'NONE',  ( 0.000000000000000000, 3.950000000000000178, 7.231250000000000178 ) ) ;
#1411=CARTESIAN_POINT ( 'NONE',  ( -0.7210596466522595227, 3.743128570366073937, 7.996158673814918849 ) ) ;
#1412=CARTESIAN_POINT ( 'NONE',  ( 0.7386972477860229702, 3.819935838229653768, 8.515578956946562528 ) ) ;
#1429=CARTESIAN_POINT ( 'NONE',  ( 0.7466433925744948574, 3.878406391858416402, 7.926888364618726257 ) ) ;
#1431=FACE_OUTER_BOUND ( 'NONE', #3309, .T. ) ;
#1449=CARTESIAN_POINT ( 'NONE',  ( -0.7386972477860230812, 3.819935838229653768, 7.946921043053440492 ) ) ;
#1464=CARTESIAN_POINT ( 'NONE',  ( 0.6866307324975363668, 3.648256581353261030, 8.149316802294766404 ) ) ;
#1492=CARTESIAN_POINT ( 'NONE',  ( 0.6863513793485908066, 3.647607376475762830, 8.312718817107960234 ) ) ;
#1511=CARTESIAN_POINT ( 'NONE',  ( 0.7431911064911158604, 4.051321384912569101, 8.527048809074747382 ) ) ;
#1535=CARTESIAN_POINT ( 'NONE',  ( 0.7370170160409607041, 3.810752038529029218, 8.511197325751680864 ) ) ;
#1577=CARTESIAN_POINT ( 'NONE',  ( -0.7122963468828453770, 3.714722057770372121, 8.437904003344627313 ) ) ;
#1583=DIRECTION ( 'NONE',  ( 0.000000000000000000, 0.000000000000000000, 1.000000000000000000 ) ) ;
#1593=CARTESIAN_POINT ( 'NONE',  ( 0.6836440906233618442, 4.258440652362253331, 8.180003846963320058 ) ) ;
#1622=PRODUCT_DEFINITION ( 'UNKNOWN', '', #4741, #378 ) ;
#1630=CARTESIAN_POINT ( 'NONE',  ( 0.6889980206436411292, 4.246403994982890673, 8.130130038714289853 ) ) ;
#1631=CONICAL_SURFACE ( 'NONE', #5024, 0.7499999999999993339, 0.7853981633974437271 ) ;
#1633=ADVANCED_FACE ( 'N', ( #5611 ), #4994, .T. ) ;
#1666=VERTEX_POINT ( 'NONE', #7777 ) ;
#1670=CARTESIAN_POINT ( 'NONE',  ( 0.7432847975395557860, 4.051926198797242584, 7.935140446388321500 ) ) ;
#1687=CARTESIAN_POINT ( 'NONE',  ( -0.6863513793485910286, 4.252392623524238857, 8.312718817107960234 ) ) ;
#1706=PRODUCT_DEFINITION_SHAPE ( 'NONE', 'NONE',  #1622 ) ;
#1724=CARTESIAN_POINT ( 'NONE',  ( -0.6892550738286248313, 4.245699673162182108, 8.129643686836866223 ) ) ;
#1732=CARTESIAN_POINT ( 'NONE',  ( 0.6000000000000015321, 3.950000000000000178, 8.981250000000001066 ) ) ;
#1764=CARTESIAN_POINT ( 'NONE',  ( -0.7314405957411594938, 4.116041651862893502, 8.496183445665876022 ) ) ;
#1841=CARTESIAN_POINT ( 'NONE',  ( -0.6817881100752513079, 4.262513956817777228, 8.241141111267666020 ) ) ;
#1850=ORIENTED_EDGE ( 'NONE', *, *, #5686, .F. ) ;
#1958=CYLINDRICAL_SURFACE ( 'NONE', #5993, 0.3125000000000016653 ) ;
#2036=CARTESIAN_POINT ( 'NONE',  ( 0.7371834602650289003, 3.810622082980045455, 7.950806627216492117 ) ) ;
#2038=CARTESIAN_POINT ( 'NONE',  ( 0.7335374419612978869, 4.107240241069344044, 8.502074107329821828 ) ) ;
#2065=DIRECTION ( 'NONE',  ( 1.000000000000000000, 0.000000000000000000, 0.000000000000000000 ) ) ;
#2080=CARTESIAN_POINT ( 'NONE',  ( 0.6907419235105255462, 3.657778167482562903, 8.120048698298123924 ) ) ;
#2092=CARTESIAN_POINT ( 'NONE',  ( 0.7499999999999993339, 3.950000000000000178, 8.831250000000000711 ) ) ;
#2098=CARTESIAN_POINT ( 'NONE',  ( -0.7499999999999993339, 3.950000000000000178, 8.231250000000001066 ) ) ;
#2106=CARTESIAN_POINT ( 'NONE',  ( 0.000000000000000000, 3.950000000000000178, 7.231250000000000178 ) ) ;
#2114=LINE ( 'NONE', #6516, #4251 ) ;
#2117=CARTESIAN_POINT ( 'NONE',  ( 0.7253671533374043134, 4.140809826333097021, 8.478940687276063315 ) ) ;
#2125=( NAMED_UNIT ( * ) SI_UNIT ( $, .STERADIAN. ) SOLID_ANGLE_UNIT ( ) );
#2138=CARTESIAN_POINT ( 'NONE',  ( 0.7432847975395561191, 3.848073801202759103, 8.527359553611677967 ) ) ;
#2140=ADVANCED_BREP_SHAPE_REPRESENTATION ( '', ( #7194, #7272 ), #1380 ) ;
#2152=CYLINDRICAL_SURFACE ( 'NONE', #4267, 0.7499999999999993339 ) ;
#2158=CARTESIAN_POINT ( 'NONE',  ( 0.7431911064911156384, 3.848678615087431698, 7.935451190925252085 ) ) ;
#2162=CLOSED_SHELL ( 'NONE', ( #8186, #5672, #5157, #840, #2803, #4474, #4173, #1633 ) ) ;
#2198=FACE_OUTER_BOUND ( 'NONE', #6529, .T. ) ;
#2255=ORIENTED_EDGE ( 'NONE', *, *, #7536, .T. ) ;
#2275=CARTESIAN_POINT ( 'NONE',  ( 0.7333924044284368948, 4.107224863919222813, 7.960989307084956224 ) ) ;
#2307=DIRECTION ( 'NONE',  ( 0.000000000000000000, 0.000000000000000000, 1.000000000000000000 ) ) ;
#2327=ORIENTED_EDGE ( 'NONE', *, *, #8052, .F. ) ;
#2411=VECTOR ( 'NONE', #2307, 39.37007874015748143 ) ;
#2425=CARTESIAN_POINT ( 'NONE',  ( -0.7457411423250318583, 4.032391550759110821, 8.533409342498828210 ) ) ;
#2426=AXIS2_PLACEMENT_3D ( 'NONE', #4239, #6053, #3553 ) ;
#2440=CARTESIAN_POINT ( 'NONE',  ( -0.6827599196736726661, 3.639582871947503850, 8.272753927050759515 ) ) ;
#2452=VERTEX_POINT ( 'NONE', #5603 ) ;
#2468=CARTESIAN_POINT ( 'NONE',  ( 0.000000000000000000, 3.950000000000000178, 8.981250000000001066 ) ) ;
#2470=CARTESIAN_POINT ( 'NONE',  ( -0.7456179150311872394, 4.031565731729908286, 7.929405685993585529 ) ) ;
#2505=CARTESIAN_POINT ( 'NONE',  ( -0.6818077110526902240, 4.262471192484426297, 8.210173163913728089 ) ) ;
#2523=CARTESIAN_POINT ( 'NONE',  ( -0.7499999999999993339, 3.929104627039255782, 8.543750000000002842 ) ) ;
#2555=ORIENTED_EDGE ( 'NONE', *, *, #943, .F. ) ;
#2585=EDGE_CURVE ( 'NONE', #1666, #5045, #4112, .T. ) ;
#2592=DIRECTION ( 'NONE',  ( 0.000000000000000000, 0.000000000000000000, -1.000000000000000000 ) ) ;
#2598=EDGE_CURVE ( 'NONE', #5045, #4460, #6562, .T. ) ;
#2655=CARTESIAN_POINT ( 'NONE',  ( 0.7417920657368231030, 3.838932697565026864, 7.938974592032494115 ) ) ;
#2699=CARTESIAN_POINT ( 'NONE',  ( 0.7274884641267199692, 4.132581358865608401, 8.485068404623115512 ) ) ;
#2730=APPLICATION_CONTEXT ( 'configuration controlled 3d designs of mechanical parts and assemblies' ) ;
#2780=SHAPE_REPRESENTATION ( 'bench vise9-', ( #7272 ), #1380 ) ;
#2803=ADVANCED_FACE ( 'NONE', ( #1431 ), #1958, .F. ) ;
#2816=CARTESIAN_POINT ( 'NONE',  ( 0.7499999999999995559, 3.970887754116599666, 7.918750000000000178 ) ) ;
#2853=CARTESIAN_POINT ( 'NONE',  ( 0.6994518761186668820, 4.220944655642501431, 8.074232055893794779 ) ) ;
#2877=EDGE_CURVE ( 'NONE', #938, #4460, #767, .T. ) ;
#2889=CARTESIAN_POINT ( 'NONE',  ( 0.7210596466522595227, 4.156871429633926418, 7.996158673814920625 ) ) ;
#2890=ORIENTED_EDGE ( 'NONE', *, *, #3027, .T. ) ;
#2906=EDGE_LOOP ( 'NONE', ( #3129, #6923, #2327, #6570 ) ) ;
#2950=CARTESIAN_POINT ( 'NONE',  ( -0.7188803599037373315, 4.163931010176847636, 8.003234414602300006 ) ) ;
#2961=ORIENTED_EDGE ( 'NONE', *, *, #6808, .T. ) ;
#2986=CARTESIAN_POINT ( 'NONE',  ( -0.6994737761126073039, 4.220893194183548580, 8.074121781180345181 ) ) ;
#3022=CARTESIAN_POINT ( 'NONE',  ( -0.6889980206436411292, 4.246403994982890673, 8.332369961285714055 ) ) ;
#3027=EDGE_CURVE ( 'NONE', #5045, #1666, #109, .T. ) ;
#3030=PLANE ( 'NONE',  #835 ) ;
#3067=ORIENTED_EDGE ( 'NONE', *, *, #3977, .T. ) ;
#3068=CARTESIAN_POINT ( 'NONE',  ( -0.6956352003900579950, 4.230470471097700802, 8.091948598562707318 ) ) ;
#3129=ORIENTED_EDGE ( 'NONE', *, *, #943, .T. ) ;
#3185=CARTESIAN_POINT ( 'NONE',  ( 0.6827599196736722220, 3.639582871947503850, 8.189746072949246170 ) ) ;
#3255=PRODUCT ( 'bench vise9-', 'bench vise9-', '', ( #6611 ) ) ;
#3263=CARTESIAN_POINT ( 'NONE',  ( 0.7499999999999995559, 3.929104627039257558, 7.918749999999998401 ) ) ;
#3286=CARTESIAN_POINT ( 'NONE',  ( -0.6889980206436411292, 3.653596005017110127, 8.130130038714286300 ) ) ;
#3309=EDGE_LOOP ( 'NONE', ( #3866, #4073, #2961, #1124 ) ) ;
#3328=CARTESIAN_POINT ( 'NONE',  ( 0.7333924044284377830, 3.792775136080777987, 8.501510692915044132 ) ) ;
#3345=DIRECTION ( 'NONE',  ( -1.000000000000000000, -0.000000000000000000, -0.000000000000000000 ) ) ;
#3369=CARTESIAN_POINT ( 'NONE',  ( 0.7253895767696342256, 3.758660869344151223, 8.479158915174224376 ) ) ;
#3377=CARTESIAN_POINT ( 'NONE',  ( -0.7253671533374044245, 3.759190173666904666, 8.478940687276063315 ) ) ;
#3389=CARTESIAN_POINT ( 'NONE',  ( 0.7491290119348462673, 3.908602837234293581, 7.920824285553323740 ) ) ;
#3428=CARTESIAN_POINT ( 'NONE',  ( 0.7491290119348464893, 3.991397162765705442, 8.541675714446673950 ) ) ;
#3470=CARTESIAN_POINT ( 'NONE',  ( 0.7078558382242214897, 4.198166876146032678, 8.422262045139364162 ) ) ;
#3496=LINE ( 'NONE', #5488, #7168 ) ;
#3513=CARTESIAN_POINT ( 'NONE',  ( 0.6956352003900579950, 4.230470471097700802, 8.370551401437293038 ) ) ;
#3553=DIRECTION ( 'NONE',  ( -1.000000000000000000, 0.000000000000000000, 0.000000000000000000 ) ) ;
#3562=CARTESIAN_POINT ( 'NONE',  ( -0.7499999999999995559, 3.970887754116599666, 8.543750000000002842 ) ) ;
#3573=CIRCLE ( 'NONE', #432, 0.6000000000000015321 ) ;
#3578=VERTEX_POINT ( 'NONE', #6957 ) ;
#3611=CARTESIAN_POINT ( 'NONE',  ( -0.7210596466522595227, 4.156871429633926418, 8.466341326185078842 ) ) ;
#3653=CARTESIAN_POINT ( 'NONE',  ( -0.7253895767696344477, 4.141339130655848244, 8.479158915174227928 ) ) ;
#3687=CARTESIAN_POINT ( 'NONE',  ( -0.7491228847736894902, 3.991630787898853949, 8.541661844804179893 ) ) ;
#3724=CARTESIAN_POINT ( 'NONE',  ( -0.6829499219002715948, 4.259968811991060811, 8.272284810380442721 ) ) ;
#3736=CARTESIAN_POINT ( 'NONE',  ( 0.000000000000000000, 0.000000000000000000, 0.000000000000000000 ) ) ;
#3766=ORIENTED_EDGE ( 'NONE', *, *, #2585, .T. ) ;
#3775=DIRECTION ( 'NONE',  ( 0.000000000000000000, 0.000000000000000000, 1.000000000000000000 ) ) ;
#3802=DIRECTION ( 'NONE',  ( 1.000000000000000000, 0.000000000000000000, 0.000000000000000000 ) ) ;
#3826=VECTOR ( 'NONE', #7566, 39.37007874015748143 ) ;
#3866=ORIENTED_EDGE ( 'NONE', *, *, #2598, .F. ) ;
#3870=CARTESIAN_POINT ( 'NONE',  ( -0.7499999999999993339, 3.950000000000000178, 8.231250000000001066 ) ) ;
#3886=CARTESIAN_POINT ( 'NONE',  ( -0.7457411423250316362, 3.867608449240891311, 7.929090657501175698 ) ) ;
#3891=CARTESIAN_POINT ( 'NONE',  ( -0.6000000000000015321, 3.950000000000000178, 8.981250000000001066 ) ) ;
#3903=CARTESIAN_POINT ( 'NONE',  ( 0.6956352003900579950, 3.669529528902299997, 8.091948598562707318 ) ) ;
#3922=CARTESIAN_POINT ( 'NONE',  ( -0.7499999999999993339, 3.950000000000000178, 7.918749999999998401 ) ) ;
#3926=CARTESIAN_POINT ( 'NONE',  ( -0.7432847975395561191, 3.848073801202759103, 7.935140446388324165 ) ) ;
#3940=CARTESIAN_POINT ( 'NONE',  ( 0.6994737761126067488, 3.679106805816449555, 8.074121781180350510 ) ) ;
#3948=VERTEX_POINT ( 'NONE', #3891 ) ;
#3956=EDGE_CURVE ( 'NONE', #2452, #938, #5141, .T. ) ;
#3971=CARTESIAN_POINT ( 'NONE',  ( 0.6889980206436410182, 3.653596005017109682, 8.332369961285712279 ) ) ;
#3977=EDGE_CURVE ( 'NONE', #8086, #3578, #7588, .T. ) ;
#3992=CARTESIAN_POINT ( 'NONE',  ( 0.7210672075785409252, 3.743534557078039615, 7.996449899345008383 ) ) ;
#3994=CARTESIAN_POINT ( 'NONE',  ( 0.7122963468828452660, 4.185277942229626902, 8.437904003344623760 ) ) ;
#4016=ORIENTED_EDGE ( 'NONE', *, *, #6238, .F. ) ;
#4017=CARTESIAN_POINT ( 'NONE',  ( -0.7314405957411597159, 3.783958348137107297, 7.966316554334126998 ) ) ;
#4022=CARTESIAN_POINT ( 'NONE',  ( -0.7210672075785413693, 3.743534557078041836, 8.466050100654991084 ) ) ;
#4050=CARTESIAN_POINT ( 'NONE',  ( -0.7491228847736897123, 3.908369212101148626, 7.920838155195822239 ) ) ;
#4062=DIRECTION ( 'NONE',  ( 1.000000000000000000, 0.000000000000000000, 0.000000000000000000 ) ) ;
#4068=CARTESIAN_POINT ( 'NONE',  ( 0.6955978521287335958, 4.230565908133124609, 8.092097759609568897 ) ) ;
#4073=ORIENTED_EDGE ( 'NONE', *, *, #2585, .F. ) ;
#4096=CARTESIAN_POINT ( 'NONE',  ( -0.6817881100752515300, 3.637486043182223572, 8.221358888732334336 ) ) ;
#4110=CARTESIAN_POINT ( 'NONE',  ( 0.7122575715994515777, 4.185397438661337510, 8.024726960321796554 ) ) ;
#4112=B_SPLINE_CURVE_WITH_KNOTS ( 'NONE', 3,
 ( #5140, #5855, #3428, #5924, #7729, #1511, #7686, #5805, #2038, #2699, #2117, #4573, #4610, #3994, #3470, #5973, #3513, #6675, #7247, #4692, #7208, #394, #977, #6010, #7860, #4728, #1593, #352, #1630, #4068, #2853, #7899, #4110, #2889, #5380, #7937, #2275, #4772, #7303, #1670, #5299, #4150, #2816, #4574 ),
 .UNSPECIFIED., .F., .F.,
 ( 4, 2, 2, 2, 2, 2, 2, 2, 2, 2, 2, 2, 2, 2, 2, 2, 2, 2, 2, 2, 2, 4 ),
 ( 0.02509446659736457724, 0.02666229889018166543, 0.02744621503659023035, 0.02823013118299879526, 0.02979796347581595978, 0.03058187962222452122, 0.03136579576863308960, 0.03293362806145024718, 0.03450146035426740476, 0.03528537650067598008, 0.03606929264708456234, 0.03763712493990171298, 0.03842104108631023973, 0.03920495723271877342, 0.04077278952553576447, 0.04234062181835274857, 0.04390845411116973268, 0.04547628640398672373, 0.04626020255039523660, 0.04704411869680374947, 0.04861195098962078215, 0.05017978328243780789 ),
 .UNSPECIFIED. ) ;
#4135=B_SPLINE_CURVE_WITH_KNOTS ( 'NONE', 3,
 ( #8037, #2523, #5474, #7392, #6250, #639, #5011, #4400, #46, #172, #3377, #4022, #6549, #1577, #6589, #4562, #7070, #8059, #1047, #4271, #8104, #2440, #4929, #4096, #7286, #5369, #7105, #4555, #3286, #7660, #7022, #5282, #7065, #1411, #7146, #4017, #4635, #7189, #1449, #3926, #3886, #4050, #823, #6542 ),
 .UNSPECIFIED., .F., .F.,
 ( 4, 2, 2, 2, 2, 2, 2, 2, 2, 2, 2, 2, 2, 2, 2, 2, 2, 2, 2, 2, 2, 4 ),
 ( 0.000000000000000000, 0.001568404162335257888, 0.002352606243502886833, 0.003136808324670516644, 0.004705212487005845656, 0.005489414568173528811, 0.006273616649341211098, 0.007842020811676602560, 0.009410424974011993154, 0.01019462705517968151, 0.01097882913634736814, 0.01254723329868273791, 0.01333143537985037944, 0.01411563746101802269, 0.01568404162335322594, 0.01725244578568842918, 0.01882084994802362896, 0.02038925411035882873, 0.02117345619152645811, 0.02195765827269408402, 0.02352606243502932890, 0.02509446659736457724 ),
 .UNSPECIFIED. ) ;
#4150=CARTESIAN_POINT ( 'NONE',  ( 0.7491228847736894902, 3.991630787898853949, 7.920838155195820462 ) ) ;
#4167=CARTESIAN_POINT ( 'NONE',  ( -0.7499999999999992228, 3.970895372960746350, 7.918749999999996625 ) ) ;
#4173=ADVANCED_FACE ( 'NONE', ( #6191 ), #3030, .T. ) ;
#4205=CARTESIAN_POINT ( 'NONE',  ( -0.6854931847115989241, 4.254309166866921288, 8.159427574546592510 ) ) ;
#4211=CARTESIAN_POINT ( 'NONE',  ( 0.7499999999999993339, 3.950000000000000178, 7.231250000000000178 ) ) ;
#4239=CARTESIAN_POINT ( 'NONE',  ( 0.000000000000000000, 3.950000000000000178, 8.831250000000000711 ) ) ;
#4251=VECTOR ( 'NONE', #3345, 39.37007874015748143 ) ;
#4263=ORIENTED_EDGE ( 'NONE', *, *, #1386, .F. ) ;
#4267=AXIS2_PLACEMENT_3D ( 'NONE', #7158, #1583, #4062 ) ;
#4271=CARTESIAN_POINT ( 'NONE',  ( -0.6866307324975363668, 3.648256581353261030, 8.313183197705237504 ) ) ;
#4299=CARTESIAN_POINT ( 'NONE',  ( -0.7432847975395557860, 4.051926198797242584, 8.527359553611677967 ) ) ;
#4333=CARTESIAN_POINT ( 'NONE',  ( -0.6994518761186668820, 4.220944655642501431, 8.388267944106205576 ) ) ;
#4343=DIRECTION ( 'NONE',  ( 1.000000000000000000, 0.000000000000000000, 0.000000000000000000 ) ) ;
#4345=ORIENTED_EDGE ( 'NONE', *, *, #6340, .F. ) ;
#4360=B_SPLINE_CURVE_WITH_KNOTS ( 'NONE', 3,
 ( #6183, #4167, #5440, #8132, #2470, #4952, #7358, #5519, #567, #453, #4835, #1111, #2950, #6688, #7322, #2986, #3068, #8006, #1724, #7494, #4205, #1224, #2505, #1841, #8046, #3724, #6228, #1687, #3022, #5569, #4333, #6840, #6066, #3611, #3653, #1764, #616, #1071, #8087, #4299, #2425, #3687, #3562, #529 ),
 .UNSPECIFIED., .F., .F.,
 ( 4, 2, 2, 2, 2, 2, 2, 2, 2, 2, 2, 2, 2, 2, 2, 2, 2, 2, 2, 2, 2, 4 ),
 ( 0.02509446659736457724, 0.02666229889018166543, 0.02744621503659023035, 0.02823013118299879526, 0.02979796347581595978, 0.03058187962222452122, 0.03136579576863308960, 0.03293362806145024718, 0.03450146035426740476, 0.03528537650067598008, 0.03606929264708456234, 0.03763712493990171298, 0.03842104108631023973, 0.03920495723271877342, 0.04077278952553576447, 0.04234062181835274857, 0.04390845411116973268, 0.04547628640398672373, 0.04626020255039523660, 0.04704411869680374947, 0.04861195098962078215, 0.05017978328243780789 ),
 .UNSPECIFIED. ) ;
#4400=CARTESIAN_POINT ( 'NONE',  ( -0.7371834602650286783, 3.810622082980043679, 8.511693372783508238 ) ) ;
#4458=CARTESIAN_POINT ( 'NONE',  ( 0.000000000000000000, 3.950000000000000178, 8.831250000000000711 ) ) ;
#4460=VERTEX_POINT ( 'NONE', #3922 ) ;
#4464=CARTESIAN_POINT ( 'NONE',  ( 0.000000000000000000, 3.950000000000000178, 7.231250000000000178 ) ) ;
#4474=ADVANCED_FACE ( 'NONE', ( #114 ), #1631, .T. ) ;
#4487=CARTESIAN_POINT ( 'NONE',  ( 0.6818077110526898910, 3.637528807515572726, 8.210173163913728089 ) ) ;
#4521=ORIENTED_EDGE ( 'NONE', *, *, #3977, .F. ) ;
#4528=AXIS2_PLACEMENT_3D ( 'NONE', #4825, #7346, #8032 ) ;
#4551=DIRECTION ( 'NONE',  ( 0.000000000000000000, 0.000000000000000000, 1.000000000000000000 ) ) ;
#4555=CARTESIAN_POINT ( 'NONE',  ( -0.6863513793485908066, 3.647607376475762386, 8.149781182892043674 ) ) ;
#4562=CARTESIAN_POINT ( 'NONE',  ( -0.6994737761126068598, 3.679106805816449999, 8.388378218819653398 ) ) ;
#4572=CARTESIAN_POINT ( 'NONE',  ( 0.6892550738286251644, 3.654300326837817359, 8.129643686836868000 ) ) ;
#4573=CARTESIAN_POINT ( 'NONE',  ( 0.7210672075785411472, 4.156465442921959408, 8.466050100654991084 ) ) ;
#4574=CARTESIAN_POINT ( 'NONE',  ( 0.7499999999999993339, 3.950000000000000178, 7.918749999999998401 ) ) ;
#4582=DIRECTION ( 'NONE',  ( -0.000000000000000000, -0.000000000000000000, -1.000000000000000000 ) ) ;
#4610=CARTESIAN_POINT ( 'NONE',  ( 0.7188803599037373315, 4.163931010176847636, 8.459265585397703902 ) ) ;
#4614=ORIENTED_EDGE ( 'NONE', *, *, #5686, .T. ) ;
#4617=( NAMED_UNIT ( * ) PLANE_ANGLE_UNIT ( ) SI_UNIT ( $, .RADIAN. ) );
#4631=EDGE_LOOP ( 'NONE', ( #4935, #2255, #798, #4016 ) ) ;
#4635=CARTESIAN_POINT ( 'NONE',  ( -0.7333924044284376720, 3.792775136080777543, 7.960989307084957112 ) ) ;
#4663=ORIENTED_EDGE ( 'NONE', *, *, #2598, .T. ) ;
#4692=CARTESIAN_POINT ( 'NONE',  ( 0.6866307324975362558, 4.251743418646740658, 8.313183197705233951 ) ) ;
#4724=EDGE_CURVE ( 'NONE', #4460, #8086, #4360, .T. ) ;
#4728=CARTESIAN_POINT ( 'NONE',  ( 0.6829499219002715948, 4.259968811991060811, 8.190215189619561187 ) ) ;
#4741=PRODUCT_DEFINITION_FORMATION_WITH_SPECIFIED_SOURCE ( 'ANY', '', #3255, .NOT_KNOWN. ) ;
#4772=CARTESIAN_POINT ( 'NONE',  ( 0.7370170160409599269, 4.089247961470974246, 7.951302674248321267 ) ) ;
#4825=CARTESIAN_POINT ( 'NONE',  ( 0.000000000000000000, 3.950000000000000178, 8.981250000000001066 ) ) ;
#4835=CARTESIAN_POINT ( 'NONE',  ( -0.7253671533374043134, 4.140809826333097021, 7.983559312723937929 ) ) ;
#4901=AXIS2_PLACEMENT_3D ( 'NONE', #4464, #3775, #4343 ) ;
#4929=CARTESIAN_POINT ( 'NONE',  ( -0.6818077110526901130, 3.637528807515573170, 8.252326836086272266 ) ) ;
#4935=ORIENTED_EDGE ( 'NONE', *, *, #6201, .F. ) ;
#4952=CARTESIAN_POINT ( 'NONE',  ( -0.7431911064911158604, 4.051321384912569101, 7.935451190925254750 ) ) ;
#4975=EDGE_LOOP ( 'NONE', ( #5985, #5353, #6166, #3067, #1121, #4345, #3766, #4263 ) ) ;
#4994=PLANE ( 'NONE',  #5457 ) ;
#5011=CARTESIAN_POINT ( 'NONE',  ( -0.7417920657368231030, 3.838932697565026864, 8.523525407967506240 ) ) ;
#5022=CARTESIAN_POINT ( 'NONE',  ( -0.7499999999999993339, 3.950000000000000178, 7.231250000000000178 ) ) ;
#5024=AXIS2_PLACEMENT_3D ( 'NONE', #6971, #2592, #5084 ) ;
#5029=AXIS2_PLACEMENT_3D ( 'NONE', #4458, #4582, #3802 ) ;
#5045=VERTEX_POINT ( 'NONE', #6528 ) ;
#5084=DIRECTION ( 'NONE',  ( -1.000000000000000000, 0.000000000000000000, 0.000000000000000000 ) ) ;
#5085=CYLINDRICAL_SURFACE ( 'NONE', #4901, 0.7499999999999993339 ) ;
#5139=CARTESIAN_POINT ( 'NONE',  ( 0.7335374419612976649, 3.792759758930657199, 7.960425892670179415 ) ) ;
#5140=CARTESIAN_POINT ( 'NONE',  ( 0.7499999999999993339, 3.950000000000000178, 8.543750000000002842 ) ) ;
#5141=CIRCLE ( 'NONE', #7121, 0.7499999999999993339 ) ;
#5152=DIRECTION ( 'NONE',  ( 0.000000000000000000, 0.000000000000000000, 1.000000000000000000 ) ) ;
#5157=ADVANCED_FACE ( 'NONE', ( #1061 ), #6209, .T. ) ;
#5162=CIRCLE ( 'NONE', #5029, 0.7499999999999993339 ) ;
#5220=CARTESIAN_POINT ( 'NONE',  ( -0.7499999999999993339, 3.950000000000000178, 7.918749999999998401 ) ) ;
#5254=CARTESIAN_POINT ( 'NONE',  ( 0.7456179150311873505, 3.868434268270091625, 7.929405685993586417 ) ) ;
#5275=AXIS2_PLACEMENT_3D ( 'NONE', #2098, #6403, #4551 ) ;
#5282=CARTESIAN_POINT ( 'NONE',  ( -0.7077600209949284071, 3.701565529548706657, 8.040603848493713457 ) ) ;
#5299=CARTESIAN_POINT ( 'NONE',  ( 0.7457411423250318583, 4.032391550759110821, 7.929090657501173034 ) ) ;
#5353=ORIENTED_EDGE ( 'NONE', *, *, #2877, .T. ) ;
#5369=CARTESIAN_POINT ( 'NONE',  ( -0.6829499219002717059, 3.640031188008939989, 8.190215189619557634 ) ) ;
#5380=CARTESIAN_POINT ( 'NONE',  ( 0.7253895767696344477, 4.141339130655848244, 7.983341084825775980 ) ) ;
#5440=CARTESIAN_POINT ( 'NONE',  ( -0.7491290119348464893, 3.991397162765705442, 7.920824285553324628 ) ) ;
#5457=AXIS2_PLACEMENT_3D ( 'NONE', #5817, #5152, #859 ) ;
#5474=CARTESIAN_POINT ( 'NONE',  ( -0.7491290119348461563, 3.908602837234294913, 8.541675714446675727 ) ) ;
#5488=CARTESIAN_POINT ( 'NONE',  ( 0.7499999999999993339, 3.950000000000000178, 7.231250000000000178 ) ) ;
#5492=LINE ( 'NONE', #1158, #826 ) ;
#5519=CARTESIAN_POINT ( 'NONE',  ( -0.7371834602650290114, 4.089377917019955788, 7.950806627216492117 ) ) ;
#5532=CARTESIAN_POINT ( 'NONE',  ( -0.7499999999999993339, 3.950000000000000622, 8.543750000000002842 ) ) ;
#5569=CARTESIAN_POINT ( 'NONE',  ( -0.6955978521287335958, 4.230565908133124609, 8.370402240390433235 ) ) ;
#5581=ORIENTED_EDGE ( 'NONE', *, *, #1200, .T. ) ;
#5603=CARTESIAN_POINT ( 'NONE',  ( 0.7499999999999993339, 3.950000000000000178, 7.231250000000000178 ) ) ;
#5611=FACE_OUTER_BOUND ( 'NONE', #70, .T. ) ;
#5618=DIRECTION ( 'NONE',  ( 1.000000000000000000, 0.000000000000000000, 0.000000000000000000 ) ) ;
#5672=ADVANCED_FACE ( 'NONE', ( #6973 ), #7062, .F. ) ;
#5686=EDGE_CURVE ( 'NONE', #938, #2452, #6202, .T. ) ;
#5702=DIRECTION ( 'NONE',  ( 0.000000000000000000, 0.000000000000000000, 1.000000000000000000 ) ) ;
#5741=ORIENTED_EDGE ( 'NONE', *, *, #6808, .F. ) ;
#5780=FACE_OUTER_BOUND ( 'NONE', #4975, .T. ) ;
#5805=CARTESIAN_POINT ( 'NONE',  ( 0.7371834602650290114, 4.089377917019955788, 8.511693372783511791 ) ) ;
#5807=CARTESIAN_POINT ( 'NONE',  ( 0.6820189411826722559, 3.637988102632602860, 8.251574762515335948 ) ) ;
#5817=CARTESIAN_POINT ( 'NONE',  ( 0.000000000000000000, 3.950000000000000178, 8.981250000000001066 ) ) ;
#5832=CARTESIAN_POINT ( 'NONE',  ( 0.7499999999999995559, 3.929097005416127164, 8.543750000000002842 ) ) ;
#5854=CARTESIAN_POINT ( 'NONE',  ( 0.7274884641267198582, 3.767418641134389290, 7.977431595376885731 ) ) ;
#5855=CARTESIAN_POINT ( 'NONE',  ( 0.7499999999999992228, 3.970895372960746350, 8.543750000000002842 ) ) ;
#5908=CARTESIAN_POINT ( 'NONE',  ( 0.6829499219002717059, 3.640031188008940433, 8.272284810380444497 ) ) ;
#5924=CARTESIAN_POINT ( 'NONE',  ( 0.7466433925744946354, 4.021593608141584397, 8.535611635381275875 ) ) ;
#5950=AXIS2_PLACEMENT_3D ( 'NONE', #1408, #5702, #1321 ) ;
#5973=CARTESIAN_POINT ( 'NONE',  ( 0.6994737761126073039, 4.220893194183548580, 8.388378218819653398 ) ) ;
#5985=ORIENTED_EDGE ( 'NONE', *, *, #3956, .T. ) ;
#5993=AXIS2_PLACEMENT_3D ( 'NONE', #3870, #685, #649 ) ;
#6010=CARTESIAN_POINT ( 'NONE',  ( 0.6817881100752513079, 4.262513956817777228, 8.221358888732334336 ) ) ;
#6039=CARTESIAN_POINT ( 'NONE',  ( 0.000000000000000000, 3.950000000000000178, 8.831250000000000711 ) ) ;
#6053=DIRECTION ( 'NONE',  ( 0.000000000000000000, 0.000000000000000000, -1.000000000000000000 ) ) ;
#6066=CARTESIAN_POINT ( 'NONE',  ( -0.7122575715994515777, 4.185397438661337510, 8.437773039678205578 ) ) ;
#6076=DIRECTION ( 'NONE',  ( -0.7071067811865442421, 0.000000000000000000, -0.7071067811865507924 ) ) ;
#6082=VECTOR ( 'NONE', #7651, 39.37007874015748143 ) ;
#6111=VECTOR ( 'NONE', #931, 39.37007874015748143 ) ;
#6135=APPLICATION_CONTEXT ( 'configuration controlled 3d designs of mechanical parts and assemblies' ) ;
#6166=ORIENTED_EDGE ( 'NONE', *, *, #4724, .T. ) ;
#6183=CARTESIAN_POINT ( 'NONE',  ( -0.7499999999999993339, 3.950000000000000178, 7.918749999999998401 ) ) ;
#6191=FACE_OUTER_BOUND ( 'NONE', #7305, .T. ) ;
#6201=EDGE_CURVE ( 'NONE', #8045, #6815, #7739, .T. ) ;
#6202=CIRCLE ( 'NONE', #5950, 0.7499999999999993339 ) ;
#6209=CONICAL_SURFACE ( 'NONE', #2426, 0.7499999999999993339, 0.7853981633974437271 ) ;
#6222=CARTESIAN_POINT ( 'NONE',  ( 0.6854931847115989241, 3.645690833133079956, 8.159427574546592510 ) ) ;
#6227=ORIENTED_EDGE ( 'NONE', *, *, #7536, .F. ) ;
#6228=CARTESIAN_POINT ( 'NONE',  ( -0.6836440906233618442, 4.258440652362253331, 8.282496153036678521 ) ) ;
#6237=DIRECTION ( 'NONE',  ( 0.000000000000000000, 0.000000000000000000, 1.000000000000000000 ) ) ;
#6238=EDGE_CURVE ( 'NONE', #6815, #3578, #5162, .T. ) ;
#6250=CARTESIAN_POINT ( 'NONE',  ( -0.7456179150311872394, 3.868434268270091625, 8.533094314006417491 ) ) ;
#6340=EDGE_CURVE ( 'NONE', #1666, #6815, #7313, .T. ) ;
#6350=DIRECTION ( 'NONE',  ( -1.000000000000000000, 0.000000000000000000, 0.000000000000000000 ) ) ;
#6397=ORIENTED_EDGE ( 'NONE', *, *, #3027, .F. ) ;
#6403=DIRECTION ( 'NONE',  ( -1.000000000000000000, -0.000000000000000000, -0.000000000000000000 ) ) ;
#6408=CARTESIAN_POINT ( 'NONE',  ( 0.7077600209949285182, 3.701565529548708433, 8.421896151506288675 ) ) ;
#6450=UNCERTAINTY_MEASURE_WITH_UNIT (LENGTH_MEASURE( 1.000000000000000082E-05 ), #7737, 'distance_accuracy_value', 'NONE');
#6486=VECTOR ( 'NONE', #6530, 39.37007874015748143 ) ;
#6516=CARTESIAN_POINT ( 'NONE',  ( -0.7499999999999993339, 3.950000000000000178, 8.543750000000002842 ) ) ;
#6528=CARTESIAN_POINT ( 'NONE',  ( 0.7499999999999993339, 3.950000000000000178, 7.918749999999998401 ) ) ;
#6529=EDGE_LOOP ( 'NONE', ( #1331, #4614, #1024, #2890, #952, #7695, #4521, #5581 ) ) ;
#6530=DIRECTION ( 'NONE',  ( 0.000000000000000000, 0.000000000000000000, 1.000000000000000000 ) ) ;
#6542=CARTESIAN_POINT ( 'NONE',  ( -0.7499999999999993339, 3.950000000000000178, 7.918749999999998401 ) ) ;
#6543=CARTESIAN_POINT ( 'NONE',  ( 0.7314405957411594938, 3.783958348137105965, 8.496183445665874245 ) ) ;
#6549=CARTESIAN_POINT ( 'NONE',  ( -0.7188803599037372205, 3.736068989823152275, 8.459265585397702125 ) ) ;
#6561=CARTESIAN_POINT ( 'NONE',  ( 0.7253671533374044245, 3.759190173666904222, 7.983559312723938817 ) ) ;
#6562=LINE ( 'NONE', #5220, #6111 ) ;
#6570=ORIENTED_EDGE ( 'NONE', *, *, #7951, .F. ) ;
#6589=CARTESIAN_POINT ( 'NONE',  ( -0.7078558382242211566, 3.701833123853966345, 8.422262045139364162 ) ) ;
#6611=MECHANICAL_CONTEXT ( 'NONE', #2730, 'mechanical' ) ;
#6675=CARTESIAN_POINT ( 'NONE',  ( 0.6907419235105254351, 4.242221832517436120, 8.342451301701874655 ) ) ;
#6688=CARTESIAN_POINT ( 'NONE',  ( -0.7122963468828452660, 4.185277942229626902, 8.024595996655373042 ) ) ;
#6734=DIRECTION ( 'NONE',  ( -0.000000000000000000, -0.000000000000000000, -1.000000000000000000 ) ) ;
#6808=EDGE_CURVE ( 'NONE', #1666, #8086, #2114, .T. ) ;
#6815=VERTEX_POINT ( 'NONE', #889 ) ;
#6840=CARTESIAN_POINT ( 'NONE',  ( -0.7077600209949282961, 4.198434470451293699, 8.421896151506285122 ) ) ;
#6923=ORIENTED_EDGE ( 'NONE', *, *, #6201, .T. ) ;
#6957=CARTESIAN_POINT ( 'NONE',  ( -0.7499999999999993339, 3.950000000000000178, 8.831250000000000711 ) ) ;
#6971=CARTESIAN_POINT ( 'NONE',  ( 0.000000000000000000, 3.950000000000000178, 8.831250000000000711 ) ) ;
#6973=FACE_OUTER_BOUND ( 'NONE', #6976, .T. ) ;
#6976=EDGE_LOOP ( 'NONE', ( #6397, #4663, #7077, #5741 ) ) ;
#7001=ORIENTED_EDGE ( 'NONE', *, *, #3956, .F. ) ;
#7022=CARTESIAN_POINT ( 'NONE',  ( -0.6994518761186669931, 3.679055344357500701, 8.074232055893794779 ) ) ;
#7023=CARTESIAN_POINT ( 'NONE',  ( 0.7210596466522596337, 3.743128570366075270, 8.466341326185078842 ) ) ;
#7062=CYLINDRICAL_SURFACE ( 'NONE', #5275, 0.3125000000000016653 ) ;
#7065=CARTESIAN_POINT ( 'NONE',  ( -0.7122575715994516887, 3.714602561338662845, 8.024726960321794778 ) ) ;
#7070=CARTESIAN_POINT ( 'NONE',  ( -0.6956352003900578840, 3.669529528902300441, 8.370551401437294814 ) ) ;
#7077=ORIENTED_EDGE ( 'NONE', *, *, #1200, .F. ) ;
#7082=CARTESIAN_POINT ( 'NONE',  ( 0.7499999999999993339, 3.950000000000000178, 7.918749999999998401 ) ) ;
#7105=CARTESIAN_POINT ( 'NONE',  ( -0.6836440906233618442, 3.641559347637748356, 8.180003846963320058 ) ) ;
#7121=AXIS2_PLACEMENT_3D ( 'NONE', #2106, #7712, #2065 ) ;
#7146=CARTESIAN_POINT ( 'NONE',  ( -0.7253895767696343366, 3.758660869344151223, 7.983341084825773315 ) ) ;
#7147=CARTESIAN_POINT ( 'NONE',  ( 0.6836440906233619552, 3.641559347637747912, 8.282496153036683850 ) ) ;
#7158=CARTESIAN_POINT ( 'NONE',  ( 0.000000000000000000, 3.950000000000000178, 7.231250000000000178 ) ) ;
#7168=VECTOR ( 'NONE', #418, 39.37007874015748143 ) ;
#7189=CARTESIAN_POINT ( 'NONE',  ( -0.7370170160409605931, 3.810752038529027885, 7.951302674248323932 ) ) ;
#7194=MANIFOLD_SOLID_BREP ( 'Imported1', #2162 ) ;
#7208=CARTESIAN_POINT ( 'NONE',  ( 0.6854931847115989241, 4.254309166866921288, 8.303072425453407845 ) ) ;
#7247=CARTESIAN_POINT ( 'NONE',  ( 0.6892550738286248313, 4.245699673162182108, 8.332856313163132356 ) ) ;
#7272=AXIS2_PLACEMENT_3D ( 'NONE', #3736, #6237, #5618 ) ;
#7286=CARTESIAN_POINT ( 'NONE',  ( -0.6820189411826723669, 3.637988102632602416, 8.210925237484662631 ) ) ;
#7303=CARTESIAN_POINT ( 'NONE',  ( 0.7386972477860228592, 4.080064161770346587, 7.946921043053440492 ) ) ;
#7305=EDGE_LOOP ( 'NONE', ( #7001, #1850 ) ) ;
#7313=LINE ( 'NONE', #7775, #6486 ) ;
#7322=CARTESIAN_POINT ( 'NONE',  ( -0.7078558382242214897, 4.198166876146032678, 8.040237954860636194 ) ) ;
#7346=DIRECTION ( 'NONE',  ( 0.000000000000000000, 0.000000000000000000, -1.000000000000000000 ) ) ;
#7358=CARTESIAN_POINT ( 'NONE',  ( -0.7417920657368231030, 4.061067302434975268, 7.938974592032496780 ) ) ;
#7392=CARTESIAN_POINT ( 'NONE',  ( -0.7466433925744946354, 3.878406391858415514, 8.535611635381275875 ) ) ;
#7494=CARTESIAN_POINT ( 'NONE',  ( -0.6866307324975362558, 4.251743418646740658, 8.149316802294766404 ) ) ;
#7536=EDGE_CURVE ( 'NONE', #8045, #3948, #3573, .T. ) ;
#7566=DIRECTION ( 'NONE',  ( 0.000000000000000000, 0.000000000000000000, 1.000000000000000000 ) ) ;
#7588=LINE ( 'NONE', #7886, #2411 ) ;
#7651=DIRECTION ( 'NONE',  ( 0.7071067811865442421, 8.659560562354893415E-17, -0.7071067811865507924 ) ) ;
#7660=CARTESIAN_POINT ( 'NONE',  ( -0.6955978521287337069, 3.669434091866875303, 8.092097759609567120 ) ) ;
#7685=CARTESIAN_POINT ( 'NONE',  ( 0.7078558382242211566, 3.701833123853966789, 8.040237954860639746 ) ) ;
#7686=CARTESIAN_POINT ( 'NONE',  ( 0.7417920657368231030, 4.061067302434975268, 8.523525407967506240 ) ) ;
#7695=ORIENTED_EDGE ( 'NONE', *, *, #6238, .T. ) ;
#7710=CARTESIAN_POINT ( 'NONE',  ( 0.7457411423250316362, 3.867608449240890867, 8.533409342498828210 ) ) ;
#7712=DIRECTION ( 'NONE',  ( 0.000000000000000000, 0.000000000000000000, 1.000000000000000000 ) ) ;
#7729=CARTESIAN_POINT ( 'NONE',  ( 0.7456179150311872394, 4.031565731729908286, 8.533094314006415715 ) ) ;
#7737=( CONVERSION_BASED_UNIT ( 'INCH', #778 ) LENGTH_UNIT ( ) NAMED_UNIT ( #8169 ) );
#7739=LINE ( 'NONE', #2092, #6082 ) ;
#7775=CARTESIAN_POINT ( 'NONE',  ( 0.7499999999999993339, 3.950000000000000178, 7.231250000000000178 ) ) ;
#7777=CARTESIAN_POINT ( 'NONE',  ( 0.7499999999999993339, 3.950000000000000178, 8.543750000000002842 ) ) ;
#7791=CARTESIAN_POINT ( 'NONE',  ( 0.6994518761186668820, 3.679055344357499813, 8.388267944106205576 ) ) ;
#7860=CARTESIAN_POINT ( 'NONE',  ( 0.6820189411826721448, 4.262011897367396607, 8.210925237484662631 ) ) ;
#7886=CARTESIAN_POINT ( 'NONE',  ( -0.7499999999999993339, 3.950000000000000178, 7.231250000000000178 ) ) ;
#7899=CARTESIAN_POINT ( 'NONE',  ( 0.7077600209949282961, 4.198434470451293699, 8.040603848493715233 ) ) ;
#7905=CARTESIAN_POINT ( 'NONE',  ( -0.7499999999999993339, 3.950000000000000178, 7.231250000000000178 ) ) ;
#7937=CARTESIAN_POINT ( 'NONE',  ( 0.7314405957411594938, 4.116041651862893502, 7.966316554334127886 ) ) ;
#7951=EDGE_CURVE ( 'NONE', #3948, #3578, #5492, .T. ) ;
#8006=CARTESIAN_POINT ( 'NONE',  ( -0.6907419235105254351, 4.242221832517436120, 8.120048698298123924 ) ) ;
#8032=DIRECTION ( 'NONE',  ( -1.000000000000000000, 0.000000000000000000, 0.000000000000000000 ) ) ;
#8037=CARTESIAN_POINT ( 'NONE',  ( -0.7499999999999993339, 3.950000000000000622, 8.543750000000002842 ) ) ;
#8045=VERTEX_POINT ( 'NONE', #1732 ) ;
#8046=CARTESIAN_POINT ( 'NONE',  ( -0.6820189411826721448, 4.262011897367396607, 8.251574762515335948 ) ) ;
#8052=EDGE_CURVE ( 'NONE', #3578, #6815, #1115, .T. ) ;
#8059=CARTESIAN_POINT ( 'NONE',  ( -0.6907419235105256572, 3.657778167482562459, 8.342451301701874655 ) ) ;
#8085=DIRECTION ( 'NONE',  ( 0.000000000000000000, 0.000000000000000000, -1.000000000000000000 ) ) ;
#8086=VERTEX_POINT ( 'NONE', #5532 ) ;
#8087=CARTESIAN_POINT ( 'NONE',  ( -0.7386972477860228592, 4.080064161770346587, 8.515578956946558975 ) ) ;
#8104=CARTESIAN_POINT ( 'NONE',  ( -0.6854931847115989241, 3.645690833133080400, 8.303072425453409622 ) ) ;
#8127=CIRCLE ( 'NONE', #4528, 0.6000000000000015321 ) ;
#8132=CARTESIAN_POINT ( 'NONE',  ( -0.7466433925744946354, 4.021593608141584397, 7.926888364618726257 ) ) ;
#8169=DIMENSIONAL_EXPONENTS ( 1.000000000000000000, 0.000000000000000000, 0.000000000000000000, 0.000000000000000000, 0.000000000000000000, 0.000000000000000000, 0.000000000000000000 ) ;
#8186=ADVANCED_FACE ( 'NONE', ( #5780 ), #5085, .T. ) ;
#8199=COLOUR_RGB('Deep Blue', 0.66274510, 0.83137255, 0.94901961);
#8200=FILL_AREA_STYLE_COLOUR('',#8199);
#8201=FILL_AREA_STYLE('',(#8200));
#8202=SURFACE_STYLE_FILL_AREA(#8201);
#8203=SURFACE_SIDE_STYLE('',(#8202));
#8204=SURFACE_STYLE_USAGE(.BOTH.,#8203);
#8205=PRESENTATION_STYLE_ASSIGNMENT((#8204));
#8249=STYLED_ITEM('',(#8205),#7194);
#8250=MECHANICAL_DESIGN_GEOMETRIC_PRESENTATION_REPRESENTATION('',(#8249),#1380);
ENDSEC;
END-ISO-10303-21;
